ISO-10303-21;
HEADER;
/* Generated by software containing ST-Developer
 * from STEP Tools, Inc. (www.steptools.com) 
 */

FILE_DESCRIPTION(
/* description */ ('Turntable on roller ring'),
/* implementation_level */ '2;1');

FILE_NAME(
/* name */ 'M4x10 Cap Screw.step',
/* time_stamp */ '2026-10-28T03:23:59-07:00',
/* author */ (''),
/* organization */ (''),
/* preprocessor_version */ 'ST-DEVELOPER v20.2',
/* originating_system */ 'Autodesk Translation Framework v15.17.0.0',
/* authorisation */ '');

FILE_SCHEMA (('AUTOMOTIVE_DESIGN { 1 0 10303 214 3 1 1 }'));
ENDSEC;

DATA;
#10=MECHANICAL_DESIGN_GEOMETRIC_PRESENTATION_REPRESENTATION('',(#663),#16281);
#492=CONICAL_SURFACE('',#9877,0.325,0.785398163397448);
#493=CONICAL_SURFACE('',#9881,0.335,0.785398163397448);
#494=CONICAL_SURFACE('',#9885,0.21,0.463647609000806);
#502=ORIENTED_CLOSED_SHELL('',*,#8407,.F.);
#506=BREP_WITH_VOIDS('Body1',#8408,(#502));
#544=SHAPE_REPRESENTATION_RELATIONSHIP('SRR','None',#16564,#599);
#599=ADVANCED_BREP_SHAPE_REPRESENTATION('',(#506),#16258);
#663=STYLED_ITEM('',(#16939),#506);
#956=FACE_BOUND('',#2358,.T.);
#1198=PLANE('',#9865);
#1199=PLANE('',#9866);
#1200=PLANE('',#9867);
#1201=PLANE('',#9868);
#1202=PLANE('',#9869);
#1203=PLANE('',#9870);
#1204=PLANE('',#9871);
#1205=PLANE('',#9872);
#1206=PLANE('',#9873);
#1207=PLANE('',#9875);
#1208=PLANE('',#9883);
#1640=FACE_OUTER_BOUND('',#2344,.T.);
#1641=FACE_OUTER_BOUND('',#2345,.T.);
#1642=FACE_OUTER_BOUND('',#2346,.T.);
#1643=FACE_OUTER_BOUND('',#2347,.T.);
#1644=FACE_OUTER_BOUND('',#2348,.T.);
#1645=FACE_OUTER_BOUND('',#2349,.T.);
#1646=FACE_OUTER_BOUND('',#2350,.T.);
#1647=FACE_OUTER_BOUND('',#2351,.T.);
#1648=FACE_OUTER_BOUND('',#2352,.T.);
#1649=FACE_OUTER_BOUND('',#2353,.T.);
#1650=FACE_OUTER_BOUND('',#2354,.T.);
#1651=FACE_OUTER_BOUND('',#2355,.T.);
#1652=FACE_OUTER_BOUND('',#2356,.T.);
#1653=FACE_OUTER_BOUND('',#2357,.T.);
#1654=FACE_OUTER_BOUND('',#2359,.T.);
#1655=FACE_OUTER_BOUND('',#2360,.T.);
#2344=EDGE_LOOP('',(#7253,#7254,#7255,#7256));
#2345=EDGE_LOOP('',(#7257,#7258,#7259,#7260));
#2346=EDGE_LOOP('',(#7261,#7262,#7263,#7264));
#2347=EDGE_LOOP('',(#7265,#7266,#7267,#7268));
#2348=EDGE_LOOP('',(#7269,#7270,#7271,#7272));
#2349=EDGE_LOOP('',(#7273,#7274,#7275,#7276));
#2350=EDGE_LOOP('',(#7277,#7278,#7279,#7280,#7281,#7282));
#2351=EDGE_LOOP('',(#7283,#7284,#7285,#7286,#7287,#7288));
#2352=EDGE_LOOP('',(#7289));
#2353=EDGE_LOOP('',(#7290));
#2354=EDGE_LOOP('',(#7291,#7292,#7293,#7294));
#2355=EDGE_LOOP('',(#7295,#7296,#7297,#7298));
#2356=EDGE_LOOP('',(#7299,#7300,#7301,#7302));
#2357=EDGE_LOOP('',(#7303));
#2358=EDGE_LOOP('',(#7304));
#2359=EDGE_LOOP('',(#7305,#7306,#7307,#7308));
#2360=EDGE_LOOP('',(#7309,#7310,#7311,#7312));
#2913=LINE('',#15246,#3396);
#2914=LINE('',#15248,#3397);
#2915=LINE('',#15250,#3398);
#2916=LINE('',#15251,#3399);
#2917=LINE('',#15254,#3400);
#2918=LINE('',#15256,#3401);
#2919=LINE('',#15257,#3402);
#2920=LINE('',#15260,#3403);
#2921=LINE('',#15262,#3404);
#2922=LINE('',#15263,#3405);
#2923=LINE('',#15266,#3406);
#2924=LINE('',#15268,#3407);
#2925=LINE('',#15269,#3408);
#2926=LINE('',#15272,#3409);
#2927=LINE('',#15274,#3410);
#2928=LINE('',#15275,#3411);
#2929=LINE('',#15277,#3412);
#2930=LINE('',#15278,#3413);
#2931=LINE('',#15290,#3414);
#2932=LINE('',#15294,#3415);
#2933=LINE('',#15298,#3416);
#2934=LINE('',#15305,#3417);
#2935=LINE('',#15307,#3418);
#3396=VECTOR('',#12272,1.);
#3397=VECTOR('',#12273,1.);
#3398=VECTOR('',#12274,1.);
#3399=VECTOR('',#12275,1.);
#3400=VECTOR('',#12278,1.);
#3401=VECTOR('',#12279,1.);
#3402=VECTOR('',#12280,1.);
#3403=VECTOR('',#12283,1.);
#3404=VECTOR('',#12284,1.);
#3405=VECTOR('',#12285,1.);
#3406=VECTOR('',#12288,1.);
#3407=VECTOR('',#12289,1.);
#3408=VECTOR('',#12290,1.);
#3409=VECTOR('',#12293,1.);
#3410=VECTOR('',#12294,1.);
#3411=VECTOR('',#12295,1.);
#3412=VECTOR('',#12298,1.);
#3413=VECTOR('',#12299,1.);
#3414=VECTOR('',#12316,0.325);
#3415=VECTOR('',#12321,0.35);
#3416=VECTOR('',#12326,0.335);
#3417=VECTOR('',#12335,0.21);
#3418=VECTOR('',#12338,0.2);
#3822=CIRCLE('',#9874,0.1954);
#3823=CIRCLE('',#9876,0.3);
#3824=CIRCLE('',#9878,0.35);
#3825=CIRCLE('',#9880,0.35);
#3826=CIRCLE('',#9882,0.32);
#3827=CIRCLE('',#9884,0.22);
#3828=CIRCLE('',#9886,0.1954);
#4486=VERTEX_POINT('',#15244);
#4487=VERTEX_POINT('',#15245);
#4488=VERTEX_POINT('',#15247);
#4489=VERTEX_POINT('',#15249);
#4490=VERTEX_POINT('',#15253);
#4491=VERTEX_POINT('',#15255);
#4492=VERTEX_POINT('',#15259);
#4493=VERTEX_POINT('',#15261);
#4494=VERTEX_POINT('',#15265);
#4495=VERTEX_POINT('',#15267);
#4496=VERTEX_POINT('',#15271);
#4497=VERTEX_POINT('',#15273);
#4498=VERTEX_POINT('',#15282);
#4499=VERTEX_POINT('',#15285);
#4500=VERTEX_POINT('',#15288);
#4501=VERTEX_POINT('',#15292);
#4502=VERTEX_POINT('',#15296);
#4503=VERTEX_POINT('',#15300);
#4504=VERTEX_POINT('',#15303);
#5437=EDGE_CURVE('',#4486,#4487,#2913,.T.);
#5438=EDGE_CURVE('',#4487,#4488,#2914,.T.);
#5439=EDGE_CURVE('',#4488,#4489,#2915,.T.);
#5440=EDGE_CURVE('',#4486,#4489,#2916,.T.);
#5441=EDGE_CURVE('',#4487,#4490,#2917,.T.);
#5442=EDGE_CURVE('',#4490,#4491,#2918,.T.);
#5443=EDGE_CURVE('',#4491,#4488,#2919,.T.);
#5444=EDGE_CURVE('',#4490,#4492,#2920,.T.);
#5445=EDGE_CURVE('',#4492,#4493,#2921,.T.);
#5446=EDGE_CURVE('',#4493,#4491,#2922,.T.);
#5447=EDGE_CURVE('',#4492,#4494,#2923,.T.);
#5448=EDGE_CURVE('',#4494,#4495,#2924,.T.);
#5449=EDGE_CURVE('',#4495,#4493,#2925,.T.);
#5450=EDGE_CURVE('',#4494,#4496,#2926,.T.);
#5451=EDGE_CURVE('',#4496,#4497,#2927,.T.);
#5452=EDGE_CURVE('',#4497,#4495,#2928,.T.);
#5453=EDGE_CURVE('',#4496,#4486,#2929,.T.);
#5454=EDGE_CURVE('',#4489,#4497,#2930,.T.);
#5455=EDGE_CURVE('',#4498,#4498,#3822,.T.);
#5456=EDGE_CURVE('',#4499,#4499,#3823,.T.);
#5457=EDGE_CURVE('',#4500,#4500,#3824,.T.);
#5458=EDGE_CURVE('',#4500,#4499,#2931,.T.);
#5459=EDGE_CURVE('',#4501,#4501,#3825,.T.);
#5460=EDGE_CURVE('',#4501,#4500,#2932,.T.);
#5461=EDGE_CURVE('',#4502,#4502,#3826,.T.);
#5462=EDGE_CURVE('',#4502,#4501,#2933,.T.);
#5463=EDGE_CURVE('',#4503,#4503,#3827,.T.);
#5464=EDGE_CURVE('',#4504,#4504,#3828,.F.);
#5465=EDGE_CURVE('',#4504,#4503,#2934,.T.);
#5466=EDGE_CURVE('',#4498,#4504,#2935,.T.);
#7253=ORIENTED_EDGE('',*,*,#5437,.T.);
#7254=ORIENTED_EDGE('',*,*,#5438,.T.);
#7255=ORIENTED_EDGE('',*,*,#5439,.T.);
#7256=ORIENTED_EDGE('',*,*,#5440,.F.);
#7257=ORIENTED_EDGE('',*,*,#5441,.T.);
#7258=ORIENTED_EDGE('',*,*,#5442,.T.);
#7259=ORIENTED_EDGE('',*,*,#5443,.T.);
#7260=ORIENTED_EDGE('',*,*,#5438,.F.);
#7261=ORIENTED_EDGE('',*,*,#5444,.T.);
#7262=ORIENTED_EDGE('',*,*,#5445,.T.);
#7263=ORIENTED_EDGE('',*,*,#5446,.T.);
#7264=ORIENTED_EDGE('',*,*,#5442,.F.);
#7265=ORIENTED_EDGE('',*,*,#5447,.T.);
#7266=ORIENTED_EDGE('',*,*,#5448,.T.);
#7267=ORIENTED_EDGE('',*,*,#5449,.T.);
#7268=ORIENTED_EDGE('',*,*,#5445,.F.);
#7269=ORIENTED_EDGE('',*,*,#5450,.T.);
#7270=ORIENTED_EDGE('',*,*,#5451,.T.);
#7271=ORIENTED_EDGE('',*,*,#5452,.T.);
#7272=ORIENTED_EDGE('',*,*,#5448,.F.);
#7273=ORIENTED_EDGE('',*,*,#5453,.T.);
#7274=ORIENTED_EDGE('',*,*,#5440,.T.);
#7275=ORIENTED_EDGE('',*,*,#5454,.T.);
#7276=ORIENTED_EDGE('',*,*,#5451,.F.);
#7277=ORIENTED_EDGE('',*,*,#5453,.F.);
#7278=ORIENTED_EDGE('',*,*,#5450,.F.);
#7279=ORIENTED_EDGE('',*,*,#5447,.F.);
#7280=ORIENTED_EDGE('',*,*,#5444,.F.);
#7281=ORIENTED_EDGE('',*,*,#5441,.F.);
#7282=ORIENTED_EDGE('',*,*,#5437,.F.);
#7283=ORIENTED_EDGE('',*,*,#5454,.F.);
#7284=ORIENTED_EDGE('',*,*,#5439,.F.);
#7285=ORIENTED_EDGE('',*,*,#5443,.F.);
#7286=ORIENTED_EDGE('',*,*,#5446,.F.);
#7287=ORIENTED_EDGE('',*,*,#5449,.F.);
#7288=ORIENTED_EDGE('',*,*,#5452,.F.);
#7289=ORIENTED_EDGE('',*,*,#5455,.F.);
#7290=ORIENTED_EDGE('',*,*,#5456,.F.);
#7291=ORIENTED_EDGE('',*,*,#5457,.F.);
#7292=ORIENTED_EDGE('',*,*,#5458,.T.);
#7293=ORIENTED_EDGE('',*,*,#5456,.T.);
#7294=ORIENTED_EDGE('',*,*,#5458,.F.);
#7295=ORIENTED_EDGE('',*,*,#5459,.F.);
#7296=ORIENTED_EDGE('',*,*,#5460,.T.);
#7297=ORIENTED_EDGE('',*,*,#5457,.T.);
#7298=ORIENTED_EDGE('',*,*,#5460,.F.);
#7299=ORIENTED_EDGE('',*,*,#5461,.F.);
#7300=ORIENTED_EDGE('',*,*,#5462,.T.);
#7301=ORIENTED_EDGE('',*,*,#5459,.T.);
#7302=ORIENTED_EDGE('',*,*,#5462,.F.);
#7303=ORIENTED_EDGE('',*,*,#5461,.T.);
#7304=ORIENTED_EDGE('',*,*,#5463,.F.);
#7305=ORIENTED_EDGE('',*,*,#5464,.F.);
#7306=ORIENTED_EDGE('',*,*,#5465,.T.);
#7307=ORIENTED_EDGE('',*,*,#5463,.T.);
#7308=ORIENTED_EDGE('',*,*,#5465,.F.);
#7309=ORIENTED_EDGE('',*,*,#5455,.T.);
#7310=ORIENTED_EDGE('',*,*,#5466,.T.);
#7311=ORIENTED_EDGE('',*,*,#5464,.T.);
#7312=ORIENTED_EDGE('',*,*,#5466,.F.);
#7815=CYLINDRICAL_SURFACE('',#9879,0.35);
#7816=CYLINDRICAL_SURFACE('',#9887,0.1954);
#8243=ADVANCED_FACE('',(#1640),#1198,.F.);
#8244=ADVANCED_FACE('',(#1641),#1199,.F.);
#8245=ADVANCED_FACE('',(#1642),#1200,.F.);
#8246=ADVANCED_FACE('',(#1643),#1201,.F.);
#8247=ADVANCED_FACE('',(#1644),#1202,.F.);
#8248=ADVANCED_FACE('',(#1645),#1203,.F.);
#8249=ADVANCED_FACE('',(#1646),#1204,.F.);
#8250=ADVANCED_FACE('',(#1647),#1205,.F.);
#8251=ADVANCED_FACE('',(#1648),#1206,.F.);
#8252=ADVANCED_FACE('',(#1649),#1207,.T.);
#8253=ADVANCED_FACE('',(#1650),#492,.T.);
#8254=ADVANCED_FACE('',(#1651),#7815,.T.);
#8255=ADVANCED_FACE('',(#1652),#493,.T.);
#8256=ADVANCED_FACE('',(#1653,#956),#1208,.T.);
#8257=ADVANCED_FACE('',(#1654),#494,.T.);
#8258=ADVANCED_FACE('',(#1655),#7816,.T.);
#8407=CLOSED_SHELL('',(#8243,#8244,#8245,#8246,#8247,#8248,#8249,#8250));
#8408=CLOSED_SHELL('',(#8251,#8252,#8253,#8254,#8255,#8256,#8257,#8258));
#9864=AXIS2_PLACEMENT_3D('',#15242,#12268,#12269);
#9865=AXIS2_PLACEMENT_3D('',#15243,#12270,#12271);
#9866=AXIS2_PLACEMENT_3D('',#15252,#12276,#12277);
#9867=AXIS2_PLACEMENT_3D('',#15258,#12281,#12282);
#9868=AXIS2_PLACEMENT_3D('',#15264,#12286,#12287);
#9869=AXIS2_PLACEMENT_3D('',#15270,#12291,#12292);
#9870=AXIS2_PLACEMENT_3D('',#15276,#12296,#12297);
#9871=AXIS2_PLACEMENT_3D('',#15279,#12300,#12301);
#9872=AXIS2_PLACEMENT_3D('',#15280,#12302,#12303);
#9873=AXIS2_PLACEMENT_3D('',#15281,#12304,#12305);
#9874=AXIS2_PLACEMENT_3D('',#15283,#12306,#12307);
#9875=AXIS2_PLACEMENT_3D('',#15284,#12308,#12309);
#9876=AXIS2_PLACEMENT_3D('',#15286,#12310,#12311);
#9877=AXIS2_PLACEMENT_3D('',#15287,#12312,#12313);
#9878=AXIS2_PLACEMENT_3D('',#15289,#12314,#12315);
#9879=AXIS2_PLACEMENT_3D('',#15291,#12317,#12318);
#9880=AXIS2_PLACEMENT_3D('',#15293,#12319,#12320);
#9881=AXIS2_PLACEMENT_3D('',#15295,#12322,#12323);
#9882=AXIS2_PLACEMENT_3D('',#15297,#12324,#12325);
#9883=AXIS2_PLACEMENT_3D('',#15299,#12327,#12328);
#9884=AXIS2_PLACEMENT_3D('',#15301,#12329,#12330);
#9885=AXIS2_PLACEMENT_3D('',#15302,#12331,#12332);
#9886=AXIS2_PLACEMENT_3D('',#15304,#12333,#12334);
#9887=AXIS2_PLACEMENT_3D('',#15306,#12336,#12337);
#12268=DIRECTION('axis',(0.,0.,1.));
#12269=DIRECTION('refdir',(1.,0.,0.));
#12270=DIRECTION('center_axis',(0.866025403784439,0.,-0.5));
#12271=DIRECTION('ref_axis',(0.5,0.,0.866025403784439));
#12272=DIRECTION('',(-0.5,0.,-0.866025403784439));
#12273=DIRECTION('',(0.,-1.,0.));
#12274=DIRECTION('',(0.5,0.,0.866025403784439));
#12275=DIRECTION('',(0.,-1.,0.));
#12276=DIRECTION('center_axis',(1.60246890531964E-16,0.,-1.));
#12277=DIRECTION('ref_axis',(1.,0.,1.60246890531964E-16));
#12278=DIRECTION('',(-1.,0.,-1.60246890531964E-16));
#12279=DIRECTION('',(0.,-1.,0.));
#12280=DIRECTION('',(1.,0.,1.60246890531964E-16));
#12281=DIRECTION('center_axis',(-0.866025403784439,0.,-0.5));
#12282=DIRECTION('ref_axis',(0.5,0.,-0.866025403784439));
#12283=DIRECTION('',(-0.5,0.,0.866025403784439));
#12284=DIRECTION('',(0.,-1.,0.));
#12285=DIRECTION('',(0.5,0.,-0.866025403784439));
#12286=DIRECTION('center_axis',(-0.866025403784439,0.,0.5));
#12287=DIRECTION('ref_axis',(-0.5,0.,-0.866025403784439));
#12288=DIRECTION('',(0.5,0.,0.866025403784439));
#12289=DIRECTION('',(0.,-1.,0.));
#12290=DIRECTION('',(-0.5,0.,-0.866025403784439));
#12291=DIRECTION('center_axis',(-1.60246890531964E-16,0.,1.));
#12292=DIRECTION('ref_axis',(-1.,0.,-1.60246890531964E-16));
#12293=DIRECTION('',(1.,0.,1.60246890531964E-16));
#12294=DIRECTION('',(0.,-1.,0.));
#12295=DIRECTION('',(-1.,0.,-1.60246890531964E-16));
#12296=DIRECTION('center_axis',(0.866025403784439,0.,0.5));
#12297=DIRECTION('ref_axis',(-0.5,0.,0.866025403784439));
#12298=DIRECTION('',(0.5,0.,-0.866025403784439));
#12299=DIRECTION('',(-0.5,0.,0.866025403784439));
#12300=DIRECTION('center_axis',(0.,1.,0.));
#12301=DIRECTION('ref_axis',(1.,0.,0.));
#12302=DIRECTION('center_axis',(0.,-1.,0.));
#12303=DIRECTION('ref_axis',(0.,0.,-1.));
#12304=DIRECTION('center_axis',(0.,1.,0.));
#12305=DIRECTION('ref_axis',(1.,0.,0.));
#12306=DIRECTION('center_axis',(0.,1.,0.));
#12307=DIRECTION('ref_axis',(1.,0.,0.));
#12308=DIRECTION('center_axis',(0.,1.,0.));
#12309=DIRECTION('ref_axis',(0.,0.,1.));
#12310=DIRECTION('center_axis',(0.,-1.,0.));
#12311=DIRECTION('ref_axis',(1.,0.,0.));
#12312=DIRECTION('center_axis',(0.,-1.,0.));
#12313=DIRECTION('ref_axis',(1.,0.,0.));
#12314=DIRECTION('center_axis',(0.,-1.,0.));
#12315=DIRECTION('ref_axis',(1.,0.,0.));
#12316=DIRECTION('',(0.707106781186547,0.707106781186548,8.65956056235493E-17));
#12317=DIRECTION('center_axis',(0.,-1.,0.));
#12318=DIRECTION('ref_axis',(1.,0.,0.));
#12319=DIRECTION('center_axis',(0.,-1.,0.));
#12320=DIRECTION('ref_axis',(1.,0.,0.));
#12321=DIRECTION('',(0.,1.,0.));
#12322=DIRECTION('center_axis',(0.,1.,0.));
#12323=DIRECTION('ref_axis',(1.,0.,0.));
#12324=DIRECTION('center_axis',(0.,-1.,0.));
#12325=DIRECTION('ref_axis',(1.,0.,0.));
#12326=DIRECTION('',(-0.707106781186547,0.707106781186548,-8.65956056235493E-17));
#12327=DIRECTION('center_axis',(0.,-1.,0.));
#12328=DIRECTION('ref_axis',(0.,0.,-1.));
#12329=DIRECTION('center_axis',(0.,-1.,0.));
#12330=DIRECTION('ref_axis',(1.,0.,0.));
#12331=DIRECTION('center_axis',(0.,1.,0.));
#12332=DIRECTION('ref_axis',(1.,0.,0.));
#12333=DIRECTION('center_axis',(0.,1.,0.));
#12334=DIRECTION('ref_axis',(1.,0.,0.));
#12335=DIRECTION('',(-0.447213595499958,0.894427190999916,-5.47678698264203E-17));
#12336=DIRECTION('center_axis',(0.,-1.,0.));
#12337=DIRECTION('ref_axis',(1.,0.,0.));
#12338=DIRECTION('',(0.,1.,0.));
#15242=CARTESIAN_POINT('',(0.,0.,0.));
#15243=CARTESIAN_POINT('Origin',(0.0866025403784439,-0.4,-0.15));
#15244=CARTESIAN_POINT('',(0.173205080756888,-0.4,0.));
#15245=CARTESIAN_POINT('',(0.0866025403784439,-0.4,-0.15));
#15246=CARTESIAN_POINT('',(0.173205080756888,-0.4,0.));
#15247=CARTESIAN_POINT('',(0.0866025403784439,-0.64,-0.15));
#15248=CARTESIAN_POINT('',(0.0866025403784439,-0.4,-0.15));
#15249=CARTESIAN_POINT('',(0.173205080756888,-0.64,0.));
#15250=CARTESIAN_POINT('',(0.173205080756888,-0.64,0.));
#15251=CARTESIAN_POINT('',(0.173205080756888,-0.4,0.));
#15252=CARTESIAN_POINT('Origin',(-0.0866025403784438,-0.4,-0.15));
#15253=CARTESIAN_POINT('',(-0.0866025403784438,-0.4,-0.15));
#15254=CARTESIAN_POINT('',(0.0866025403784439,-0.4,-0.15));
#15255=CARTESIAN_POINT('',(-0.0866025403784438,-0.64,-0.15));
#15256=CARTESIAN_POINT('',(-0.0866025403784438,-0.4,-0.15));
#15257=CARTESIAN_POINT('',(0.0866025403784439,-0.64,-0.15));
#15258=CARTESIAN_POINT('Origin',(-0.173205080756888,-0.4,-2.77555756156289E-17));
#15259=CARTESIAN_POINT('',(-0.173205080756888,-0.4,-2.12115047744981E-17));
#15260=CARTESIAN_POINT('',(-0.0866025403784438,-0.4,-0.15));
#15261=CARTESIAN_POINT('',(-0.173205080756888,-0.64,-2.77555756156289E-17));
#15262=CARTESIAN_POINT('',(-0.173205080756888,-0.4,-2.12115047744981E-17));
#15263=CARTESIAN_POINT('',(-0.0866025403784438,-0.64,-0.15));
#15264=CARTESIAN_POINT('Origin',(-0.0866025403784439,-0.4,0.15));
#15265=CARTESIAN_POINT('',(-0.0866025403784439,-0.4,0.15));
#15266=CARTESIAN_POINT('',(-0.173205080756888,-0.4,-2.12115047744981E-17));
#15267=CARTESIAN_POINT('',(-0.0866025403784439,-0.64,0.15));
#15268=CARTESIAN_POINT('',(-0.0866025403784439,-0.4,0.15));
#15269=CARTESIAN_POINT('',(-0.173205080756888,-0.64,-2.12115047744981E-17));
#15270=CARTESIAN_POINT('Origin',(0.0866025403784439,-0.4,0.15));
#15271=CARTESIAN_POINT('',(0.0866025403784439,-0.4,0.15));
#15272=CARTESIAN_POINT('',(-0.0866025403784439,-0.4,0.15));
#15273=CARTESIAN_POINT('',(0.0866025403784439,-0.64,0.15));
#15274=CARTESIAN_POINT('',(0.0866025403784439,-0.4,0.15));
#15275=CARTESIAN_POINT('',(-0.0866025403784439,-0.64,0.15));
#15276=CARTESIAN_POINT('Origin',(0.173205080756888,-0.4,0.));
#15277=CARTESIAN_POINT('',(0.0866025403784439,-0.4,0.15));
#15278=CARTESIAN_POINT('',(0.0866025403784439,-0.64,0.15));
#15279=CARTESIAN_POINT('Origin',(0.,-0.4,-2.77555756156289E-17));
#15280=CARTESIAN_POINT('Origin',(0.,-0.64,-2.77555756156289E-17));
#15281=CARTESIAN_POINT('Origin',(0.,-1.,0.));
#15282=CARTESIAN_POINT('',(-0.1954,-1.,2.39295984553393E-17));
#15283=CARTESIAN_POINT('Origin',(0.,-1.,0.));
#15284=CARTESIAN_POINT('Origin',(0.3,0.4,0.));
#15285=CARTESIAN_POINT('',(-0.3,0.4,-3.67394039744206E-17));
#15286=CARTESIAN_POINT('Origin',(0.,0.4,0.));
#15287=CARTESIAN_POINT('Origin',(0.,0.375,0.));
#15288=CARTESIAN_POINT('',(-0.35,0.35,-4.28626379701573E-17));
#15289=CARTESIAN_POINT('Origin',(0.,0.35,0.));
#15290=CARTESIAN_POINT('',(-0.325,0.375,-3.9801020972289E-17));
#15291=CARTESIAN_POINT('Origin',(0.,0.19,0.));
#15292=CARTESIAN_POINT('',(-0.35,0.03,-4.28626379701574E-17));
#15293=CARTESIAN_POINT('Origin',(0.,0.03,0.));
#15294=CARTESIAN_POINT('',(-0.35,0.19,-4.28626379701574E-17));
#15295=CARTESIAN_POINT('Origin',(0.,0.0149999999999999,0.));
#15296=CARTESIAN_POINT('',(-0.32,-3.29597460435593E-17,-3.91886975727153E-17));
#15297=CARTESIAN_POINT('Origin',(0.,0.,0.));
#15298=CARTESIAN_POINT('',(-0.335,0.0149999999999999,-4.10256677714363E-17));
#15299=CARTESIAN_POINT('Origin',(0.22,0.,0.));
#15300=CARTESIAN_POINT('',(-0.22,-6.93889390390723E-18,-2.69422295812418E-17));
#15301=CARTESIAN_POINT('Origin',(0.,0.,0.));
#15302=CARTESIAN_POINT('Origin',(0.,-0.02,0.));
#15303=CARTESIAN_POINT('',(-0.1954,-0.0492,2.39295984553393E-17));
#15304=CARTESIAN_POINT('Origin',(0.,-0.0492,0.));
#15305=CARTESIAN_POINT('',(-0.21,-0.02,-2.57175827820944E-17));
#15306=CARTESIAN_POINT('Origin',(0.,-0.8,0.));
#15307=CARTESIAN_POINT('',(-0.1954,-0.8,-2.39295984553393E-17));
#16189=UNCERTAINTY_MEASURE_WITH_UNIT(LENGTH_MEASURE(0.001),#16282,
'DISTANCE_ACCURACY_VALUE',
'Maximum model space distance between geometric entities at asserted c
onnectivities');
#16212=UNCERTAINTY_MEASURE_WITH_UNIT(LENGTH_MEASURE(0.001),#16282,
'DISTANCE_ACCURACY_VALUE',
'Maximum model space distance between geometric entities at asserted c
onnectivities');
#16258=(
GEOMETRIC_REPRESENTATION_CONTEXT(3)
GLOBAL_UNCERTAINTY_ASSIGNED_CONTEXT((#16189))
GLOBAL_UNIT_ASSIGNED_CONTEXT((#16282,#16284,#16285))
REPRESENTATION_CONTEXT('','3D')
);
#16281=(
GEOMETRIC_REPRESENTATION_CONTEXT(3)
GLOBAL_UNCERTAINTY_ASSIGNED_CONTEXT((#16212))
GLOBAL_UNIT_ASSIGNED_CONTEXT((#16282,#16284,#16285))
REPRESENTATION_CONTEXT('','3D')
);
#16282=(
LENGTH_UNIT()
NAMED_UNIT(*)
SI_UNIT(.CENTI.,.METRE.)
);
#16284=(
NAMED_UNIT(*)
PLANE_ANGLE_UNIT()
SI_UNIT($,.RADIAN.)
);
#16285=(
NAMED_UNIT(*)
SI_UNIT($,.STERADIAN.)
SOLID_ANGLE_UNIT()
);
#16331=SHAPE_DEFINITION_REPRESENTATION(#16425,#16564);
#16425=PRODUCT_DEFINITION_SHAPE('',$,#16633);
#16564=SHAPE_REPRESENTATION('',(#9864),#16258);
#16587=PRODUCT_DEFINITION_CONTEXT('part definition',#16793,'design');
#16633=PRODUCT_DEFINITION('M4x10 Cap Screw','M4x10 Cap Screw',#16701,#16587);
#16701=PRODUCT_DEFINITION_FORMATION('',$,#16840);
#16793=APPLICATION_CONTEXT(
'Core Data for Automotive Mechanical Design Process');
#16794=PRODUCT_CONTEXT('part definition',#16793,'mechanical');
#16840=PRODUCT('M4x10 Cap Screw','M4x10 Cap Screw','M4x10 Cap Screw',(#16794));
#16933=COLOUR_RGB('Black',0.12,0.14,0.17);
#16934=FILL_AREA_STYLE_COLOUR('',#16933);
#16935=FILL_AREA_STYLE('',(#16934));
#16936=SURFACE_STYLE_FILL_AREA(#16935);
#16937=SURFACE_SIDE_STYLE('',(#16936));
#16938=SURFACE_STYLE_USAGE(.BOTH.,#16937);
#16939=PRESENTATION_STYLE_ASSIGNMENT((#16938));
ENDSEC;
END-ISO-10303-21;
